ISO-10303-21;
HEADER;
FILE_DESCRIPTION (('STEP AP214'),
    '1' );
FILE_NAME ('plain washer 10669 type nl_iso_ISO 10669-5.4-N.step',
    '2026-10-27T08:02:39',
    ( '' ),
    ( '' ),
    'SwSTEP 2.0',
    'SolidWorks 2026',
    '' );
FILE_SCHEMA (( 'AUTOMOTIVE_DESIGN' ));
ENDSEC;

DATA;
#12=UNCERTAINTY_MEASURE_WITH_UNIT (LENGTH_MEASURE( 1.000000000000000082E-05 ), #6900, 'distance_accuracy_value', 'NONE');
#59=ADVANCED_FACE ( 'NONE', ( #10781 ), #4214, .F. ) ;
#113=SURFACE_STYLE_FILL_AREA ( #10791 ) ;
#159=PLANE ( 'NONE',  #4576 ) ;
#161=CARTESIAN_POINT ( 'NONE',  ( 0.000000000000000000, 0.000000000000000000, 0.000000000000000000 ) ) ;
#212=CARTESIAN_POINT ( 'NONE',  ( 0.000000000000000000, 0.000000000000000000, 0.000000000000000000 ) ) ;
#221=DIRECTION ( 'NONE',  ( -1.000000000000000000, -0.000000000000000000, -0.000000000000000000 ) ) ;
#258=AXIS2_PLACEMENT_3D ( 'NONE', #11179, #11120, #1690 ) ;
#353=VERTEX_POINT ( 'NONE', #11740 ) ;
#421=FACE_OUTER_BOUND ( 'NONE', #899, .T. ) ;
#600=ORIENTED_EDGE ( 'NONE', *, *, #5405, .T. ) ;
#616=AXIS2_PLACEMENT_3D ( 'NONE', #161, #1107, #1158 ) ;
#672=APPLICATION_CONTEXT ( 'automotive_design' ) ;
#708=CARTESIAN_POINT ( 'NONE',  ( 1.600000000000000089, 0.000000000000000000, 7.000000000000000000 ) ) ;
#767=AXIS2_PLACEMENT_3D ( 'NONE', #1245, #5249, #6889 ) ;
#899=EDGE_LOOP ( 'NONE', ( #6133, #4541, #600, #8975 ) ) ;
#1017=UNCERTAINTY_MEASURE_WITH_UNIT (LENGTH_MEASURE( 1.000000000000000082E-05 ), #6880, 'distance_accuracy_value', 'NONE');
#1064=AXIS2_PLACEMENT_3D ( 'NONE', #11381, #6768, #9579 ) ;
#1107=DIRECTION ( 'NONE',  ( 1.000000000000000000, 0.000000000000000000, 0.000000000000000000 ) ) ;
#1113=( NAMED_UNIT ( * ) PLANE_ANGLE_UNIT ( ) SI_UNIT ( $, .RADIAN. ) );
#1158=DIRECTION ( 'NONE',  ( 0.000000000000000000, 0.000000000000000000, -1.000000000000000000 ) ) ;
#1162=PRESENTATION_STYLE_ASSIGNMENT (( #3984 ) ) ;
#1209=DIRECTION ( 'NONE',  ( 1.000000000000000000, 0.000000000000000000, 0.000000000000000000 ) ) ;
#1233=( NAMED_UNIT ( * ) PLANE_ANGLE_UNIT ( ) SI_UNIT ( $, .RADIAN. ) );
#1245=CARTESIAN_POINT ( 'NONE',  ( 0.000000000000000000, 0.000000000000000000, 0.000000000000000000 ) ) ;
#1293=( LENGTH_UNIT ( ) NAMED_UNIT ( * ) SI_UNIT ( .MILLI., .METRE. ) );
#1544=SHAPE_REPRESENTATION ( 'plain washer 10669 type nl_iso_ISO 10669-5.4-N', ( #6056 ), #8843 ) ;
#1602=EDGE_CURVE ( 'NONE', #9064, #11240, #2549, .T. ) ;
#1690=DIRECTION ( 'NONE',  ( 0.000000000000000000, 0.000000000000000000, -1.000000000000000000 ) ) ;
#1786=VECTOR ( 'NONE', #7800, 1000.000000000000000 ) ;
#1788=AXIS2_PLACEMENT_3D ( 'NONE', #7262, #6361, #9366 ) ;
#1822=AXIS2_PLACEMENT_3D ( 'NONE', #5485, #6599, #10406 ) ;
#1859=CIRCLE ( 'NONE', #1064, 2.700000000000000178 ) ;
#1960=CARTESIAN_POINT ( 'NONE',  ( 1.600000000000000089, 0.000000000000000000, 0.000000000000000000 ) ) ;
#1994=DIRECTION ( 'NONE',  ( 1.000000000000000000, 0.000000000000000000, 0.000000000000000000 ) ) ;
#2050=CARTESIAN_POINT ( 'NONE',  ( 1.600000000000000089, 0.000000000000000000, 2.700000000000000178 ) ) ;
#2171=APPLICATION_CONTEXT ( 'automotive_design' ) ;
#2198=PRODUCT_DEFINITION ( 'UNKNOWN', '', #4236, #7024 ) ;
#2282=ORIENTED_EDGE ( 'NONE', *, *, #8010, .F. ) ;
#2316=LINE ( 'NONE', #9718, #4372 ) ;
#2549=CIRCLE ( 'NONE', #10753, 2.700000000000000178 ) ;
#2564=ADVANCED_BREP_SHAPE_REPRESENTATION ( '', ( #8778, #6056 ), #8843 ) ;
#2611=CARTESIAN_POINT ( 'NONE',  ( 1.600000000000000089, 0.000000000000000000, 0.000000000000000000 ) ) ;
#2680=FACE_BOUND ( 'NONE', #10736, .T. ) ;
#2721=ORIENTED_EDGE ( 'NONE', *, *, #1602, .F. ) ;
#2760=ORIENTED_EDGE ( 'NONE', *, *, #3569, .T. ) ;
#2835=ORIENTED_EDGE ( 'NONE', *, *, #7796, .F. ) ;
#3505=AXIS2_PLACEMENT_3D ( 'NONE', #6750, #1994, #6626 ) ;
#3559=AXIS2_PLACEMENT_3D ( 'NONE', #2611, #7375, #11914 ) ;
#3569=EDGE_CURVE ( 'NONE', #11219, #7247, #4846, .T. ) ;
#3920=LINE ( 'NONE', #2050, #1786 ) ;
#3974=ORIENTED_EDGE ( 'NONE', *, *, #1602, .T. ) ;
#3984=SURFACE_STYLE_USAGE ( .BOTH. , #6057 ) ;
#4035=DIRECTION ( 'NONE',  ( 0.000000000000000000, 0.000000000000000000, 1.000000000000000000 ) ) ;
#4112=FILL_AREA_STYLE_COLOUR ( '', #9845 ) ;
#4214=CYLINDRICAL_SURFACE ( 'NONE', #7587, 2.700000000000000178 ) ;
#4236=PRODUCT_DEFINITION_FORMATION_WITH_SPECIFIED_SOURCE ( 'ANY', '', #6516, .NOT_KNOWN. ) ;
#4300=EDGE_LOOP ( 'NONE', ( #7317, #3974 ) ) ;
#4372=VECTOR ( 'NONE', #6905, 1000.000000000000000 ) ;
#4420=ORIENTED_EDGE ( 'NONE', *, *, #5405, .F. ) ;
#4469=CYLINDRICAL_SURFACE ( 'NONE', #8190, 2.700000000000000178 ) ;
#4541=ORIENTED_EDGE ( 'NONE', *, *, #3569, .F. ) ;
#4576=AXIS2_PLACEMENT_3D ( 'NONE', #11417, #5978, #9684 ) ;
#4683=PLANE ( 'NONE',  #3505 ) ;
#4766=FACE_OUTER_BOUND ( 'NONE', #9935, .T. ) ;
#4846=CIRCLE ( 'NONE', #258, 7.000000000000000000 ) ;
#4885=ADVANCED_FACE ( 'NONE', ( #4766 ), #8589, .T. ) ;
#4899=UNCERTAINTY_MEASURE_WITH_UNIT (LENGTH_MEASURE( 1.000000000000000082E-05 ), #1293, 'distance_accuracy_value', 'NONE');
#5054=( NAMED_UNIT ( * ) SI_UNIT ( $, .STERADIAN. ) SOLID_ANGLE_UNIT ( ) );
#5100=VECTOR ( 'NONE', #9371, 1000.000000000000000 ) ;
#5101=DIRECTION ( 'NONE',  ( 0.000000000000000000, 0.000000000000000000, 1.000000000000000000 ) ) ;
#5109=SHAPE_REPRESENTATION_RELATIONSHIP ( 'NONE' , 'NONE' ,  #1544, #2564 ) ;
#5249=DIRECTION ( 'NONE',  ( 1.000000000000000000, 0.000000000000000000, 0.000000000000000000 ) ) ;
#5405=EDGE_CURVE ( 'NONE', #11219, #353, #9707, .T. ) ;
#5485=CARTESIAN_POINT ( 'NONE',  ( 1.600000000000000089, 0.000000000000000000, 0.000000000000000000 ) ) ;
#5522=CARTESIAN_POINT ( 'NONE',  ( 0.000000000000000000, 0.000000000000000000, 2.700000000000000178 ) ) ;
#5548=EDGE_LOOP ( 'NONE', ( #8795, #6483 ) ) ;
#5576=CIRCLE ( 'NONE', #7183, 2.700000000000000178 ) ;
#5687=ADVANCED_FACE ( 'NONE', ( #11484, #2680 ), #4683, .T. ) ;
#5700=EDGE_CURVE ( 'NONE', #7247, #8440, #10431, .T. ) ;
#5913=CARTESIAN_POINT ( 'NONE',  ( 0.000000000000000000, 0.000000000000000000, 0.000000000000000000 ) ) ;
#5978=DIRECTION ( 'NONE',  ( 1.000000000000000000, 0.000000000000000000, 0.000000000000000000 ) ) ;
#5987=CLOSED_SHELL ( 'NONE', ( #59, #4885, #5687, #7949, #10675, #8306 ) ) ;
#5999=EDGE_LOOP ( 'NONE', ( #10242, #10287, #11061, #2282 ) ) ;
#6011=STYLED_ITEM('',(#12405),#8778);
#6030=CIRCLE ( 'NONE', #616, 7.000000000000000000 ) ;
#6056=AXIS2_PLACEMENT_3D ( 'NONE', #212, #4035, #8864 ) ;
#6057=SURFACE_SIDE_STYLE ('',( #113 ) ) ;
#6133=ORIENTED_EDGE ( 'NONE', *, *, #5700, .F. ) ;
#6172=CIRCLE ( 'NONE', #767, 7.000000000000000000 ) ;
#6216=MECHANICAL_DESIGN_GEOMETRIC_PRESENTATION_REPRESENTATION('',(#6011),#7813);
#6361=DIRECTION ( 'NONE',  ( -1.000000000000000000, -0.000000000000000000, -0.000000000000000000 ) ) ;
#6425=CARTESIAN_POINT ( 'NONE',  ( 1.600000000000000089, 8.572527594031473190E-16, -7.000000000000000000 ) ) ;
#6479=DIRECTION ( 'NONE',  ( -1.000000000000000000, -0.000000000000000000, -0.000000000000000000 ) ) ;
#6483=ORIENTED_EDGE ( 'NONE', *, *, #9065, .F. ) ;
#6516=PRODUCT ( 'plain washer 10669 type nl_iso_ISO 10669-5.4-N', 'plain washer 10669 type nl_iso_ISO 10669-5.4-N', '', ( #8487 ) ) ;
#6599=DIRECTION ( 'NONE',  ( 1.000000000000000000, 0.000000000000000000, 0.000000000000000000 ) ) ;
#6620=DIRECTION ( 'NONE',  ( 0.000000000000000000, 0.000000000000000000, -1.000000000000000000 ) ) ;
#6626=DIRECTION ( 'NONE',  ( 0.000000000000000000, 0.000000000000000000, -1.000000000000000000 ) ) ;
#6665=DIRECTION ( 'NONE',  ( -1.000000000000000000, -0.000000000000000000, -0.000000000000000000 ) ) ;
#6721=ORIENTED_EDGE ( 'NONE', *, *, #6794, .F. ) ;
#6750=CARTESIAN_POINT ( 'NONE',  ( 1.600000000000000089, 0.000000000000000000, 0.000000000000000000 ) ) ;
#6768=DIRECTION ( 'NONE',  ( 1.000000000000000000, 0.000000000000000000, 0.000000000000000000 ) ) ;
#6794=EDGE_CURVE ( 'NONE', #7247, #11219, #9582, .T. ) ;
#6873=CARTESIAN_POINT ( 'NONE',  ( 0.000000000000000000, 3.306546357697853733E-16, -2.700000000000000178 ) ) ;
#6880=( LENGTH_UNIT ( ) NAMED_UNIT ( * ) SI_UNIT ( .MILLI., .METRE. ) );
#6889=DIRECTION ( 'NONE',  ( 0.000000000000000000, 0.000000000000000000, -1.000000000000000000 ) ) ;
#6900=( LENGTH_UNIT ( ) NAMED_UNIT ( * ) SI_UNIT ( .MILLI., .METRE. ) );
#6905=DIRECTION ( 'NONE',  ( -1.000000000000000000, -0.000000000000000000, -0.000000000000000000 ) ) ;
#6970=VERTEX_POINT ( 'NONE', #7506 ) ;
#7024=PRODUCT_DEFINITION_CONTEXT ( 'detailed design', #672, 'design' ) ;
#7080=( NAMED_UNIT ( * ) SI_UNIT ( $, .STERADIAN. ) SOLID_ANGLE_UNIT ( ) );
#7183=AXIS2_PLACEMENT_3D ( 'NONE', #11479, #10543, #6620 ) ;
#7221=CARTESIAN_POINT ( 'NONE',  ( 1.600000000000000089, 0.000000000000000000, 2.700000000000000178 ) ) ;
#7225=EDGE_LOOP ( 'NONE', ( #2835, #9090, #12051, #2721 ) ) ;
#7247=VERTEX_POINT ( 'NONE', #6425 ) ;
#7262=CARTESIAN_POINT ( 'NONE',  ( 1.600000000000000089, 0.000000000000000000, 0.000000000000000000 ) ) ;
#7317=ORIENTED_EDGE ( 'NONE', *, *, #10006, .T. ) ;
#7375=DIRECTION ( 'NONE',  ( 1.000000000000000000, 0.000000000000000000, 0.000000000000000000 ) ) ;
#7412=DIRECTION ( 'NONE',  ( 0.000000000000000000, 0.000000000000000000, 1.000000000000000000 ) ) ;
#7506=CARTESIAN_POINT ( 'NONE',  ( 1.600000000000000089, 3.306546357697853733E-16, -2.700000000000000178 ) ) ;
#7587=AXIS2_PLACEMENT_3D ( 'NONE', #9055, #221, #5101 ) ;
#7624=VERTEX_POINT ( 'NONE', #7221 ) ;
#7651=( GEOMETRIC_REPRESENTATION_CONTEXT ( 3 ) GLOBAL_UNCERTAINTY_ASSIGNED_CONTEXT ( ( #4899 ) ) GLOBAL_UNIT_ASSIGNED_CONTEXT ( ( #1293, #1113, #11535 ) ) REPRESENTATION_CONTEXT ( 'NONE', 'WORKASPACE' ) );
#7694=EDGE_LOOP ( 'NONE', ( #2760, #10536 ) ) ;
#7696=AXIS2_PLACEMENT_3D ( 'NONE', #1960, #6665, #8528 ) ;
#7796=EDGE_CURVE ( 'NONE', #6970, #9064, #2316, .T. ) ;
#7800=DIRECTION ( 'NONE',  ( -1.000000000000000000, -0.000000000000000000, -0.000000000000000000 ) ) ;
#7813=( GEOMETRIC_REPRESENTATION_CONTEXT ( 3 ) GLOBAL_UNCERTAINTY_ASSIGNED_CONTEXT ( ( #12 ) ) GLOBAL_UNIT_ASSIGNED_CONTEXT ( ( #6900, #8836, #7080 ) ) REPRESENTATION_CONTEXT ( 'NONE', 'WORKASPACE' ) );
#7828=CARTESIAN_POINT ( 'NONE',  ( 1.600000000000000089, 0.000000000000000000, 7.000000000000000000 ) ) ;
#7873=FACE_OUTER_BOUND ( 'NONE', #5548, .T. ) ;
#7949=ADVANCED_FACE ( 'NONE', ( #7873, #11662 ), #159, .F. ) ;
#7989=ORIENTED_EDGE ( 'NONE', *, *, #5700, .T. ) ;
#8010=EDGE_CURVE ( 'NONE', #7624, #11240, #3920, .T. ) ;
#8148=ORIENTED_EDGE ( 'NONE', *, *, #9065, .T. ) ;
#8190=AXIS2_PLACEMENT_3D ( 'NONE', #9166, #6479, #7412 ) ;
#8306=ADVANCED_FACE ( 'NONE', ( #10156 ), #4469, .F. ) ;
#8353=SHAPE_DEFINITION_REPRESENTATION ( #10622, #1544 ) ;
#8440=VERTEX_POINT ( 'NONE', #11515 ) ;
#8487=PRODUCT_CONTEXT ( 'NONE', #2171, 'mechanical' ) ;
#8504=CARTESIAN_POINT ( 'NONE',  ( 1.600000000000000089, 8.572527594031473190E-16, -7.000000000000000000 ) ) ;
#8528=DIRECTION ( 'NONE',  ( 0.000000000000000000, 0.000000000000000000, 1.000000000000000000 ) ) ;
#8589=CYLINDRICAL_SURFACE ( 'NONE', #7696, 7.000000000000000000 ) ;
#8778=MANIFOLD_SOLID_BREP ( 'Base-Extrude', #5987 ) ;
#8795=ORIENTED_EDGE ( 'NONE', *, *, #10662, .F. ) ;
#8836=( NAMED_UNIT ( * ) PLANE_ANGLE_UNIT ( ) SI_UNIT ( $, .RADIAN. ) );
#8843=( GEOMETRIC_REPRESENTATION_CONTEXT ( 3 ) GLOBAL_UNCERTAINTY_ASSIGNED_CONTEXT ( ( #1017 ) ) GLOBAL_UNIT_ASSIGNED_CONTEXT ( ( #6880, #1233, #5054 ) ) REPRESENTATION_CONTEXT ( 'NONE', 'WORKASPACE' ) );
#8864=DIRECTION ( 'NONE',  ( 1.000000000000000000, 0.000000000000000000, 0.000000000000000000 ) ) ;
#8975=ORIENTED_EDGE ( 'NONE', *, *, #10662, .T. ) ;
#9055=CARTESIAN_POINT ( 'NONE',  ( 1.600000000000000089, 0.000000000000000000, 0.000000000000000000 ) ) ;
#9064=VERTEX_POINT ( 'NONE', #6873 ) ;
#9065=EDGE_CURVE ( 'NONE', #8440, #353, #6030, .T. ) ;
#9090=ORIENTED_EDGE ( 'NONE', *, *, #10953, .T. ) ;
#9166=CARTESIAN_POINT ( 'NONE',  ( 1.600000000000000089, 0.000000000000000000, 0.000000000000000000 ) ) ;
#9366=DIRECTION ( 'NONE',  ( 0.000000000000000000, 0.000000000000000000, 1.000000000000000000 ) ) ;
#9371=DIRECTION ( 'NONE',  ( -1.000000000000000000, -0.000000000000000000, -0.000000000000000000 ) ) ;
#9447=CIRCLE ( 'NONE', #1822, 2.700000000000000178 ) ;
#9579=DIRECTION ( 'NONE',  ( 0.000000000000000000, 0.000000000000000000, -1.000000000000000000 ) ) ;
#9582=CIRCLE ( 'NONE', #3559, 7.000000000000000000 ) ;
#9684=DIRECTION ( 'NONE',  ( 0.000000000000000000, 0.000000000000000000, -1.000000000000000000 ) ) ;
#9707=LINE ( 'NONE', #7828, #11867 ) ;
#9718=CARTESIAN_POINT ( 'NONE',  ( 1.600000000000000089, 3.306546357697853733E-16, -2.700000000000000178 ) ) ;
#9845=COLOUR_RGB ( '',1.000000000000000000, 0.9490196078431372140, 0.9098039215686274384 ) ;
#9935=EDGE_LOOP ( 'NONE', ( #6721, #7989, #8148, #4420 ) ) ;
#10006=EDGE_CURVE ( 'NONE', #11240, #9064, #1859, .T. ) ;
#10156=FACE_OUTER_BOUND ( 'NONE', #7225, .T. ) ;
#10242=ORIENTED_EDGE ( 'NONE', *, *, #12293, .T. ) ;
#10287=ORIENTED_EDGE ( 'NONE', *, *, #7796, .T. ) ;
#10404=ORIENTED_EDGE ( 'NONE', *, *, #12293, .F. ) ;
#10406=DIRECTION ( 'NONE',  ( 0.000000000000000000, 0.000000000000000000, -1.000000000000000000 ) ) ;
#10431=LINE ( 'NONE', #8504, #5100 ) ;
#10536=ORIENTED_EDGE ( 'NONE', *, *, #6794, .T. ) ;
#10543=DIRECTION ( 'NONE',  ( 1.000000000000000000, 0.000000000000000000, 0.000000000000000000 ) ) ;
#10622=PRODUCT_DEFINITION_SHAPE ( 'NONE', 'NONE',  #2198 ) ;
#10638=DIRECTION ( 'NONE',  ( -1.000000000000000000, -0.000000000000000000, -0.000000000000000000 ) ) ;
#10662=EDGE_CURVE ( 'NONE', #353, #8440, #6172, .T. ) ;
#10675=ADVANCED_FACE ( 'NONE', ( #421 ), #11858, .T. ) ;
#10736=EDGE_LOOP ( 'NONE', ( #10404, #11383 ) ) ;
#10753=AXIS2_PLACEMENT_3D ( 'NONE', #5913, #1209, #10895 ) ;
#10781=FACE_OUTER_BOUND ( 'NONE', #5999, .T. ) ;
#10791=FILL_AREA_STYLE ('',( #4112 ) ) ;
#10815=STYLED_ITEM ( 'NONE', ( #1162 ), #2564 ) ;
#10895=DIRECTION ( 'NONE',  ( 0.000000000000000000, 0.000000000000000000, -1.000000000000000000 ) ) ;
#10953=EDGE_CURVE ( 'NONE', #6970, #7624, #5576, .T. ) ;
#11061=ORIENTED_EDGE ( 'NONE', *, *, #10006, .F. ) ;
#11120=DIRECTION ( 'NONE',  ( 1.000000000000000000, 0.000000000000000000, 0.000000000000000000 ) ) ;
#11179=CARTESIAN_POINT ( 'NONE',  ( 1.600000000000000089, 0.000000000000000000, 0.000000000000000000 ) ) ;
#11213=MECHANICAL_DESIGN_GEOMETRIC_PRESENTATION_REPRESENTATION('',(#10815),#7651);
#11219=VERTEX_POINT ( 'NONE', #708 ) ;
#11240=VERTEX_POINT ( 'NONE', #5522 ) ;
#11381=CARTESIAN_POINT ( 'NONE',  ( 0.000000000000000000, 0.000000000000000000, 0.000000000000000000 ) ) ;
#11383=ORIENTED_EDGE ( 'NONE', *, *, #10953, .F. ) ;
#11417=CARTESIAN_POINT ( 'NONE',  ( 0.000000000000000000, 0.000000000000000000, 0.000000000000000000 ) ) ;
#11479=CARTESIAN_POINT ( 'NONE',  ( 1.600000000000000089, 0.000000000000000000, 0.000000000000000000 ) ) ;
#11484=FACE_OUTER_BOUND ( 'NONE', #7694, .T. ) ;
#11515=CARTESIAN_POINT ( 'NONE',  ( 0.000000000000000000, 8.572527594031473190E-16, -7.000000000000000000 ) ) ;
#11535=( NAMED_UNIT ( * ) SI_UNIT ( $, .STERADIAN. ) SOLID_ANGLE_UNIT ( ) );
#11662=FACE_BOUND ( 'NONE', #4300, .T. ) ;
#11740=CARTESIAN_POINT ( 'NONE',  ( 0.000000000000000000, 0.000000000000000000, 7.000000000000000000 ) ) ;
#11858=CYLINDRICAL_SURFACE ( 'NONE', #1788, 7.000000000000000000 ) ;
#11867=VECTOR ( 'NONE', #10638, 1000.000000000000000 ) ;
#11914=DIRECTION ( 'NONE',  ( 0.000000000000000000, 0.000000000000000000, -1.000000000000000000 ) ) ;
#12051=ORIENTED_EDGE ( 'NONE', *, *, #8010, .T. ) ;
#12293=EDGE_CURVE ( 'NONE', #7624, #6970, #9447, .T. ) ;
#12399=COLOUR_RGB('Black',0.12,0.14,0.17);
#12400=FILL_AREA_STYLE_COLOUR('',#12399);
#12401=FILL_AREA_STYLE('',(#12400));
#12402=SURFACE_STYLE_FILL_AREA(#12401);
#12403=SURFACE_SIDE_STYLE('',(#12402));
#12404=SURFACE_STYLE_USAGE(.BOTH.,#12403);
#12405=PRESENTATION_STYLE_ASSIGNMENT((#12404));
ENDSEC;
END-ISO-10303-21;
